ISO-10303-21;
HEADER;
/* Generated by software containing ST-Developer
 * from STEP Tools, Inc. (www.steptools.com) 
 */

FILE_DESCRIPTION(
/* description */ ('PAT-096'),
/* implementation_level */ '2;1');

FILE_NAME(
/* name */ 'M4x4 collar screw.step',
/* time_stamp */ '2026-10-29T17:03:14-07:00',
/* author */ (''),
/* organization */ (''),
/* preprocessor_version */ 'ST-DEVELOPER v20.2',
/* originating_system */ 'Autodesk Translation Framework v15.17.0.0',
/* authorisation */ '');

FILE_SCHEMA (('AUTOMOTIVE_DESIGN { 1 0 10303 214 3 1 1 }'));
ENDSEC;

DATA;
#10=MECHANICAL_DESIGN_GEOMETRIC_PRESENTATION_REPRESENTATION('',(#423),#10650);
#326=CONICAL_SURFACE('',#6388,0.185,0.785398163397449);
#353=SHAPE_REPRESENTATION_RELATIONSHIP('SRR','None',#10815,#384);
#384=ADVANCED_BREP_SHAPE_REPRESENTATION('',(#460),#10633);
#423=STYLED_ITEM('',(#11071),#460);
#460=MANIFOLD_SOLID_BREP('Body1',#5558);
#558=FACE_BOUND('',#1434,.T.);
#716=PLANE('',#6377);
#717=PLANE('',#6379);
#718=PLANE('',#6380);
#719=PLANE('',#6381);
#720=PLANE('',#6382);
#721=PLANE('',#6383);
#722=PLANE('',#6384);
#723=PLANE('',#6385);
#724=PLANE('',#6386);
#1004=FACE_OUTER_BOUND('',#1425,.T.);
#1005=FACE_OUTER_BOUND('',#1426,.T.);
#1006=FACE_OUTER_BOUND('',#1427,.T.);
#1007=FACE_OUTER_BOUND('',#1428,.T.);
#1008=FACE_OUTER_BOUND('',#1429,.T.);
#1009=FACE_OUTER_BOUND('',#1430,.T.);
#1010=FACE_OUTER_BOUND('',#1431,.T.);
#1011=FACE_OUTER_BOUND('',#1432,.T.);
#1012=FACE_OUTER_BOUND('',#1433,.T.);
#1013=FACE_OUTER_BOUND('',#1435,.T.);
#1014=FACE_OUTER_BOUND('',#1436,.T.);
#1425=EDGE_LOOP('',(#4613));
#1426=EDGE_LOOP('',(#4614,#4615,#4616,#4617));
#1427=EDGE_LOOP('',(#4618,#4619,#4620,#4621));
#1428=EDGE_LOOP('',(#4622,#4623,#4624,#4625));
#1429=EDGE_LOOP('',(#4626,#4627,#4628,#4629));
#1430=EDGE_LOOP('',(#4630,#4631,#4632,#4633));
#1431=EDGE_LOOP('',(#4634,#4635,#4636,#4637));
#1432=EDGE_LOOP('',(#4638,#4639,#4640,#4641,#4642,#4643));
#1433=EDGE_LOOP('',(#4644));
#1434=EDGE_LOOP('',(#4645,#4646,#4647,#4648,#4649,#4650));
#1435=EDGE_LOOP('',(#4651,#4652,#4653,#4654));
#1436=EDGE_LOOP('',(#4655,#4656,#4657,#4658));
#1798=LINE('',#10001,#2127);
#1799=LINE('',#10003,#2128);
#1800=LINE('',#10005,#2129);
#1801=LINE('',#10006,#2130);
#1802=LINE('',#10009,#2131);
#1803=LINE('',#10011,#2132);
#1804=LINE('',#10012,#2133);
#1805=LINE('',#10015,#2134);
#1806=LINE('',#10017,#2135);
#1807=LINE('',#10018,#2136);
#1808=LINE('',#10021,#2137);
#1809=LINE('',#10023,#2138);
#1810=LINE('',#10024,#2139);
#1811=LINE('',#10027,#2140);
#1812=LINE('',#10029,#2141);
#1813=LINE('',#10030,#2142);
#1814=LINE('',#10032,#2143);
#1815=LINE('',#10033,#2144);
#1816=LINE('',#10041,#2145);
#1817=LINE('',#10043,#2146);
#2127=VECTOR('',#7798,1.);
#2128=VECTOR('',#7799,1.);
#2129=VECTOR('',#7800,1.);
#2130=VECTOR('',#7801,1.);
#2131=VECTOR('',#7804,1.);
#2132=VECTOR('',#7805,1.);
#2133=VECTOR('',#7806,1.);
#2134=VECTOR('',#7809,1.);
#2135=VECTOR('',#7810,1.);
#2136=VECTOR('',#7811,1.);
#2137=VECTOR('',#7814,1.);
#2138=VECTOR('',#7815,1.);
#2139=VECTOR('',#7816,1.);
#2140=VECTOR('',#7819,1.);
#2141=VECTOR('',#7820,1.);
#2142=VECTOR('',#7821,1.);
#2143=VECTOR('',#7824,1.);
#2144=VECTOR('',#7825,1.);
#2145=VECTOR('',#7836,0.185);
#2146=VECTOR('',#7839,0.2);
#2480=CIRCLE('',#6378,0.1954);
#2481=CIRCLE('',#6387,0.17);
#2482=CIRCLE('',#6389,0.1954);
#2884=VERTEX_POINT('',#9996);
#2885=VERTEX_POINT('',#9999);
#2886=VERTEX_POINT('',#10000);
#2887=VERTEX_POINT('',#10002);
#2888=VERTEX_POINT('',#10004);
#2889=VERTEX_POINT('',#10008);
#2890=VERTEX_POINT('',#10010);
#2891=VERTEX_POINT('',#10014);
#2892=VERTEX_POINT('',#10016);
#2893=VERTEX_POINT('',#10020);
#2894=VERTEX_POINT('',#10022);
#2895=VERTEX_POINT('',#10026);
#2896=VERTEX_POINT('',#10028);
#2897=VERTEX_POINT('',#10036);
#2898=VERTEX_POINT('',#10039);
#3485=EDGE_CURVE('',#2884,#2884,#2480,.T.);
#3486=EDGE_CURVE('',#2885,#2886,#1798,.T.);
#3487=EDGE_CURVE('',#2885,#2887,#1799,.T.);
#3488=EDGE_CURVE('',#2887,#2888,#1800,.T.);
#3489=EDGE_CURVE('',#2886,#2888,#1801,.T.);
#3490=EDGE_CURVE('',#2889,#2885,#1802,.T.);
#3491=EDGE_CURVE('',#2889,#2890,#1803,.T.);
#3492=EDGE_CURVE('',#2890,#2887,#1804,.T.);
#3493=EDGE_CURVE('',#2891,#2889,#1805,.T.);
#3494=EDGE_CURVE('',#2891,#2892,#1806,.T.);
#3495=EDGE_CURVE('',#2892,#2890,#1807,.T.);
#3496=EDGE_CURVE('',#2893,#2891,#1808,.T.);
#3497=EDGE_CURVE('',#2893,#2894,#1809,.T.);
#3498=EDGE_CURVE('',#2894,#2892,#1810,.T.);
#3499=EDGE_CURVE('',#2895,#2893,#1811,.T.);
#3500=EDGE_CURVE('',#2895,#2896,#1812,.T.);
#3501=EDGE_CURVE('',#2896,#2894,#1813,.T.);
#3502=EDGE_CURVE('',#2886,#2895,#1814,.T.);
#3503=EDGE_CURVE('',#2888,#2896,#1815,.T.);
#3504=EDGE_CURVE('',#2897,#2897,#2481,.T.);
#3505=EDGE_CURVE('',#2898,#2898,#2482,.T.);
#3506=EDGE_CURVE('',#2898,#2897,#1816,.T.);
#3507=EDGE_CURVE('',#2884,#2898,#1817,.T.);
#4613=ORIENTED_EDGE('',*,*,#3485,.F.);
#4614=ORIENTED_EDGE('',*,*,#3486,.F.);
#4615=ORIENTED_EDGE('',*,*,#3487,.T.);
#4616=ORIENTED_EDGE('',*,*,#3488,.T.);
#4617=ORIENTED_EDGE('',*,*,#3489,.F.);
#4618=ORIENTED_EDGE('',*,*,#3490,.F.);
#4619=ORIENTED_EDGE('',*,*,#3491,.T.);
#4620=ORIENTED_EDGE('',*,*,#3492,.T.);
#4621=ORIENTED_EDGE('',*,*,#3487,.F.);
#4622=ORIENTED_EDGE('',*,*,#3493,.F.);
#4623=ORIENTED_EDGE('',*,*,#3494,.T.);
#4624=ORIENTED_EDGE('',*,*,#3495,.T.);
#4625=ORIENTED_EDGE('',*,*,#3491,.F.);
#4626=ORIENTED_EDGE('',*,*,#3496,.F.);
#4627=ORIENTED_EDGE('',*,*,#3497,.T.);
#4628=ORIENTED_EDGE('',*,*,#3498,.T.);
#4629=ORIENTED_EDGE('',*,*,#3494,.F.);
#4630=ORIENTED_EDGE('',*,*,#3499,.F.);
#4631=ORIENTED_EDGE('',*,*,#3500,.T.);
#4632=ORIENTED_EDGE('',*,*,#3501,.T.);
#4633=ORIENTED_EDGE('',*,*,#3497,.F.);
#4634=ORIENTED_EDGE('',*,*,#3502,.F.);
#4635=ORIENTED_EDGE('',*,*,#3489,.T.);
#4636=ORIENTED_EDGE('',*,*,#3503,.T.);
#4637=ORIENTED_EDGE('',*,*,#3500,.F.);
#4638=ORIENTED_EDGE('',*,*,#3503,.F.);
#4639=ORIENTED_EDGE('',*,*,#3488,.F.);
#4640=ORIENTED_EDGE('',*,*,#3492,.F.);
#4641=ORIENTED_EDGE('',*,*,#3495,.F.);
#4642=ORIENTED_EDGE('',*,*,#3498,.F.);
#4643=ORIENTED_EDGE('',*,*,#3501,.F.);
#4644=ORIENTED_EDGE('',*,*,#3504,.F.);
#4645=ORIENTED_EDGE('',*,*,#3486,.T.);
#4646=ORIENTED_EDGE('',*,*,#3502,.T.);
#4647=ORIENTED_EDGE('',*,*,#3499,.T.);
#4648=ORIENTED_EDGE('',*,*,#3496,.T.);
#4649=ORIENTED_EDGE('',*,*,#3493,.T.);
#4650=ORIENTED_EDGE('',*,*,#3490,.T.);
#4651=ORIENTED_EDGE('',*,*,#3505,.F.);
#4652=ORIENTED_EDGE('',*,*,#3506,.T.);
#4653=ORIENTED_EDGE('',*,*,#3504,.T.);
#4654=ORIENTED_EDGE('',*,*,#3506,.F.);
#4655=ORIENTED_EDGE('',*,*,#3485,.T.);
#4656=ORIENTED_EDGE('',*,*,#3507,.T.);
#4657=ORIENTED_EDGE('',*,*,#3505,.T.);
#4658=ORIENTED_EDGE('',*,*,#3507,.F.);
#5151=CYLINDRICAL_SURFACE('',#6390,0.1954);
#5409=ADVANCED_FACE('',(#1004),#716,.F.);
#5410=ADVANCED_FACE('',(#1005),#717,.F.);
#5411=ADVANCED_FACE('',(#1006),#718,.F.);
#5412=ADVANCED_FACE('',(#1007),#719,.F.);
#5413=ADVANCED_FACE('',(#1008),#720,.F.);
#5414=ADVANCED_FACE('',(#1009),#721,.F.);
#5415=ADVANCED_FACE('',(#1010),#722,.F.);
#5416=ADVANCED_FACE('',(#1011),#723,.F.);
#5417=ADVANCED_FACE('',(#1012,#558),#724,.T.);
#5418=ADVANCED_FACE('',(#1013),#326,.T.);
#5419=ADVANCED_FACE('',(#1014),#5151,.T.);
#5558=CLOSED_SHELL('',(#5409,#5410,#5411,#5412,#5413,#5414,#5415,#5416,
#5417,#5418,#5419));
#6376=AXIS2_PLACEMENT_3D('',#9994,#7790,#7791);
#6377=AXIS2_PLACEMENT_3D('',#9995,#7792,#7793);
#6378=AXIS2_PLACEMENT_3D('',#9997,#7794,#7795);
#6379=AXIS2_PLACEMENT_3D('',#9998,#7796,#7797);
#6380=AXIS2_PLACEMENT_3D('',#10007,#7802,#7803);
#6381=AXIS2_PLACEMENT_3D('',#10013,#7807,#7808);
#6382=AXIS2_PLACEMENT_3D('',#10019,#7812,#7813);
#6383=AXIS2_PLACEMENT_3D('',#10025,#7817,#7818);
#6384=AXIS2_PLACEMENT_3D('',#10031,#7822,#7823);
#6385=AXIS2_PLACEMENT_3D('',#10034,#7826,#7827);
#6386=AXIS2_PLACEMENT_3D('',#10035,#7828,#7829);
#6387=AXIS2_PLACEMENT_3D('',#10037,#7830,#7831);
#6388=AXIS2_PLACEMENT_3D('',#10038,#7832,#7833);
#6389=AXIS2_PLACEMENT_3D('',#10040,#7834,#7835);
#6390=AXIS2_PLACEMENT_3D('',#10042,#7837,#7838);
#7790=DIRECTION('axis',(0.,0.,1.));
#7791=DIRECTION('refdir',(1.,0.,0.));
#7792=DIRECTION('center_axis',(0.,1.,0.));
#7793=DIRECTION('ref_axis',(1.,0.,0.));
#7794=DIRECTION('center_axis',(0.,1.,0.));
#7795=DIRECTION('ref_axis',(1.,0.,0.));
#7796=DIRECTION('center_axis',(0.866025403784439,0.,-0.5));
#7797=DIRECTION('ref_axis',(0.5,0.,0.866025403784439));
#7798=DIRECTION('',(0.5,0.,0.866025403784439));
#7799=DIRECTION('',(0.,-1.,0.));
#7800=DIRECTION('',(0.5,0.,0.866025403784439));
#7801=DIRECTION('',(0.,-1.,0.));
#7802=DIRECTION('center_axis',(1.20185167898973E-16,0.,-1.));
#7803=DIRECTION('ref_axis',(1.,0.,1.20185167898973E-16));
#7804=DIRECTION('',(1.,0.,1.20185167898973E-16));
#7805=DIRECTION('',(0.,-1.,0.));
#7806=DIRECTION('',(1.,0.,1.20185167898973E-16));
#7807=DIRECTION('center_axis',(-0.866025403784439,0.,-0.5));
#7808=DIRECTION('ref_axis',(0.5,0.,-0.866025403784439));
#7809=DIRECTION('',(0.5,0.,-0.866025403784439));
#7810=DIRECTION('',(0.,-1.,0.));
#7811=DIRECTION('',(0.5,0.,-0.866025403784439));
#7812=DIRECTION('center_axis',(-0.866025403784439,0.,0.5));
#7813=DIRECTION('ref_axis',(-0.5,0.,-0.866025403784439));
#7814=DIRECTION('',(-0.5,0.,-0.866025403784439));
#7815=DIRECTION('',(0.,-1.,0.));
#7816=DIRECTION('',(-0.5,0.,-0.866025403784439));
#7817=DIRECTION('center_axis',(-2.40370335797945E-16,0.,1.));
#7818=DIRECTION('ref_axis',(-1.,0.,-2.40370335797945E-16));
#7819=DIRECTION('',(-1.,0.,-2.40370335797945E-16));
#7820=DIRECTION('',(0.,-1.,0.));
#7821=DIRECTION('',(-1.,0.,-2.40370335797945E-16));
#7822=DIRECTION('center_axis',(0.866025403784439,0.,0.5));
#7823=DIRECTION('ref_axis',(-0.5,0.,0.866025403784439));
#7824=DIRECTION('',(-0.5,0.,0.866025403784439));
#7825=DIRECTION('',(-0.5,0.,0.866025403784439));
#7826=DIRECTION('center_axis',(0.,-1.,0.));
#7827=DIRECTION('ref_axis',(0.,0.,-1.));
#7828=DIRECTION('center_axis',(0.,1.,0.));
#7829=DIRECTION('ref_axis',(0.,0.,1.));
#7830=DIRECTION('center_axis',(0.,-1.,0.));
#7831=DIRECTION('ref_axis',(1.,0.,0.));
#7832=DIRECTION('center_axis',(0.,-1.,0.));
#7833=DIRECTION('ref_axis',(1.,0.,0.));
#7834=DIRECTION('center_axis',(0.,-1.,0.));
#7835=DIRECTION('ref_axis',(1.,0.,0.));
#7836=DIRECTION('',(0.707106781186548,0.707106781186547,8.65956056235494E-17));
#7837=DIRECTION('center_axis',(0.,-1.,0.));
#7838=DIRECTION('ref_axis',(1.,0.,0.));
#7839=DIRECTION('',(0.,1.,0.));
#9994=CARTESIAN_POINT('',(0.,0.,0.));
#9995=CARTESIAN_POINT('Origin',(0.,-0.4,0.));
#9996=CARTESIAN_POINT('',(-0.1954,-0.4,2.39295984553393E-17));
#9997=CARTESIAN_POINT('Origin',(0.,-0.4,0.));
#9998=CARTESIAN_POINT('Origin',(0.0577350269189626,0.,-0.1));
#9999=CARTESIAN_POINT('',(0.0577350269189626,0.,-0.1));
#10000=CARTESIAN_POINT('',(0.115470053837925,0.,0.));
#10001=CARTESIAN_POINT('',(0.0934187836487032,0.,-0.0381939203391614));
#10002=CARTESIAN_POINT('',(0.0577350269189626,-0.2,-0.1));
#10003=CARTESIAN_POINT('',(0.0577350269189626,0.,-0.1));
#10004=CARTESIAN_POINT('',(0.115470053837925,-0.2,0.));
#10005=CARTESIAN_POINT('',(0.115470053837925,-0.2,0.));
#10006=CARTESIAN_POINT('',(0.115470053837925,0.,0.));
#10007=CARTESIAN_POINT('Origin',(-0.0577350269189626,0.,-0.1));
#10008=CARTESIAN_POINT('',(-0.0577350269189626,0.,-0.1));
#10009=CARTESIAN_POINT('',(0.0561324865405187,0.,-0.1));
#10010=CARTESIAN_POINT('',(-0.0577350269189626,-0.2,-0.1));
#10011=CARTESIAN_POINT('',(-0.0577350269189626,0.,-0.1));
#10012=CARTESIAN_POINT('',(0.0577350269189626,-0.2,-0.1));
#10013=CARTESIAN_POINT('Origin',(-0.115470053837925,0.,-1.38777878078145E-17));
#10014=CARTESIAN_POINT('',(-0.115470053837925,0.,-1.41410031829988E-17));
#10015=CARTESIAN_POINT('',(-0.0797862971081845,0.,-0.0618060796608387));
#10016=CARTESIAN_POINT('',(-0.115470053837925,-0.2,-1.38777878078145E-17));
#10017=CARTESIAN_POINT('',(-0.115470053837925,0.,-1.41410031829988E-17));
#10018=CARTESIAN_POINT('',(-0.0577350269189626,-0.2,-0.1));
#10019=CARTESIAN_POINT('Origin',(-0.0577350269189626,0.,0.1));
#10020=CARTESIAN_POINT('',(-0.0577350269189626,0.,0.1));
#10021=CARTESIAN_POINT('',(-0.0509187836487033,0.,0.111806079660839));
#10022=CARTESIAN_POINT('',(-0.0577350269189626,-0.2,0.1));
#10023=CARTESIAN_POINT('',(-0.0577350269189626,0.,0.1));
#10024=CARTESIAN_POINT('',(-0.115470053837925,-0.2,-1.41410031829988E-17));
#10025=CARTESIAN_POINT('Origin',(0.0577350269189626,0.,0.1));
#10026=CARTESIAN_POINT('',(0.0577350269189626,0.,0.1));
#10027=CARTESIAN_POINT('',(0.113867513459481,0.,0.1));
#10028=CARTESIAN_POINT('',(0.0577350269189626,-0.2,0.1));
#10029=CARTESIAN_POINT('',(0.0577350269189626,0.,0.1));
#10030=CARTESIAN_POINT('',(-0.0577350269189626,-0.2,0.1));
#10031=CARTESIAN_POINT('Origin',(0.115470053837925,0.,0.));
#10032=CARTESIAN_POINT('',(0.122286297108185,0.,-0.0118060796608386));
#10033=CARTESIAN_POINT('',(0.0577350269189626,-0.2,0.1));
#10034=CARTESIAN_POINT('Origin',(0.,-0.2,0.));
#10035=CARTESIAN_POINT('Origin',(0.17,0.,0.));
#10036=CARTESIAN_POINT('',(-0.17,-8.67361737988404E-18,-2.0818995585505E-17));
#10037=CARTESIAN_POINT('Origin',(0.,0.,0.));
#10038=CARTESIAN_POINT('Origin',(0.,-0.015,0.));
#10039=CARTESIAN_POINT('',(-0.1954,-0.0254,-2.39295984553393E-17));
#10040=CARTESIAN_POINT('Origin',(0.,-0.0254,0.));
#10041=CARTESIAN_POINT('',(-0.185,-0.015,-2.2655965784226E-17));
#10042=CARTESIAN_POINT('Origin',(0.,-0.2775,0.));
#10043=CARTESIAN_POINT('',(-0.1954,-0.2775,-2.39295984553393E-17));
#10594=UNCERTAINTY_MEASURE_WITH_UNIT(LENGTH_MEASURE(0.001),#10651,
'DISTANCE_ACCURACY_VALUE',
'Maximum model space distance between geometric entities at asserted c
onnectivities');
#10611=UNCERTAINTY_MEASURE_WITH_UNIT(LENGTH_MEASURE(0.001),#10651,
'DISTANCE_ACCURACY_VALUE',
'Maximum model space distance between geometric entities at asserted c
onnectivities');
#10633=(
GEOMETRIC_REPRESENTATION_CONTEXT(3)
GLOBAL_UNCERTAINTY_ASSIGNED_CONTEXT((#10594))
GLOBAL_UNIT_ASSIGNED_CONTEXT((#10651,#10653,#10654))
REPRESENTATION_CONTEXT('','3D')
);
#10650=(
GEOMETRIC_REPRESENTATION_CONTEXT(3)
GLOBAL_UNCERTAINTY_ASSIGNED_CONTEXT((#10611))
GLOBAL_UNIT_ASSIGNED_CONTEXT((#10651,#10653,#10654))
REPRESENTATION_CONTEXT('','3D')
);
#10651=(
LENGTH_UNIT()
NAMED_UNIT(*)
SI_UNIT(.CENTI.,.METRE.)
);
#10653=(
NAMED_UNIT(*)
PLANE_ANGLE_UNIT()
SI_UNIT($,.RADIAN.)
);
#10654=(
NAMED_UNIT(*)
SI_UNIT($,.STERADIAN.)
SOLID_ANGLE_UNIT()
);
#10676=SHAPE_DEFINITION_REPRESENTATION(#10719,#10815);
#10719=PRODUCT_DEFINITION_SHAPE('',$,#10854);
#10815=SHAPE_REPRESENTATION('',(#6376),#10633);
#10832=PRODUCT_DEFINITION_CONTEXT('part definition',#10948,'design');
#10854=PRODUCT_DEFINITION('M4x4 collar screw','M4x4 collar screw',#10892,
#10832);
#10892=PRODUCT_DEFINITION_FORMATION('',$,#10971);
#10948=APPLICATION_CONTEXT(
'Core Data for Automotive Mechanical Design Process');
#10949=PRODUCT_CONTEXT('part definition',#10948,'mechanical');
#10971=PRODUCT('M4x4 collar screw','M4x4 collar screw',
'M4x4 collar screw',(#10949));
#11065=COLOUR_RGB('Black',0.12,0.14,0.17);
#11066=FILL_AREA_STYLE_COLOUR('',#11065);
#11067=FILL_AREA_STYLE('',(#11066));
#11068=SURFACE_STYLE_FILL_AREA(#11067);
#11069=SURFACE_SIDE_STYLE('',(#11068));
#11070=SURFACE_STYLE_USAGE(.BOTH.,#11069);
#11071=PRESENTATION_STYLE_ASSIGNMENT((#11070));
ENDSEC;
END-ISO-10303-21;
